ISO-10303-21;
HEADER;
/* Generated by software containing ST-Developer
 * from STEP Tools, Inc. (www.steptools.com) 
 */

FILE_DESCRIPTION(
/* description */ ('PAT-091'),
/* implementation_level */ '2;1');

FILE_NAME(
/* name */ 'M4 low-profile retaining screw (6).step',
/* time_stamp */ '2026-10-27T15:34:44-07:00',
/* author */ (''),
/* organization */ (''),
/* preprocessor_version */ 'ST-DEVELOPER v20.2',
/* originating_system */ 'Autodesk Translation Framework v15.17.0.0',
/* authorisation */ '');

FILE_SCHEMA (('AUTOMOTIVE_DESIGN { 1 0 10303 214 3 1 1 }'));
ENDSEC;

DATA;
#10=MECHANICAL_DESIGN_GEOMETRIC_PRESENTATION_REPRESENTATION('',(#1055),#25100);
#835=SHAPE_REPRESENTATION_RELATIONSHIP('SRR','None',#25602,#945);
#945=ADVANCED_BREP_SHAPE_REPRESENTATION('',(#1176),#25072);
#1055=STYLED_ITEM('',(#26198),#1176);
#1176=MANIFOLD_SOLID_BREP('Body1',#13335);
#1569=FACE_BOUND('',#3857,.T.);
#1980=PLANE('',#15933);
#1981=PLANE('',#15938);
#1982=PLANE('',#15941);
#2684=FACE_OUTER_BOUND('',#3856,.T.);
#2685=FACE_OUTER_BOUND('',#3858,.T.);
#2686=FACE_OUTER_BOUND('',#3859,.T.);
#2687=FACE_OUTER_BOUND('',#3860,.T.);
#2688=FACE_OUTER_BOUND('',#3861,.T.);
#3856=EDGE_LOOP('',(#11402));
#3857=EDGE_LOOP('',(#11403));
#3858=EDGE_LOOP('',(#11404,#11405,#11406,#11407));
#3859=EDGE_LOOP('',(#11408));
#3860=EDGE_LOOP('',(#11409,#11410,#11411,#11412));
#3861=EDGE_LOOP('',(#11413));
#4775=LINE('',#23843,#5515);
#4776=LINE('',#23847,#5516);
#5515=VECTOR('',#19825,0.350000000000001);
#5516=VECTOR('',#19830,0.199999999999999);
#6164=CIRCLE('',#15934,0.350000000000001);
#6165=CIRCLE('',#15935,0.199999999999999);
#6166=CIRCLE('',#15937,0.350000000000001);
#6167=CIRCLE('',#15940,0.199999999999999);
#7189=VERTEX_POINT('',#23836);
#7190=VERTEX_POINT('',#23838);
#7191=VERTEX_POINT('',#23841);
#7192=VERTEX_POINT('',#23846);
#8636=EDGE_CURVE('',#7189,#7189,#6164,.T.);
#8637=EDGE_CURVE('',#7190,#7190,#6165,.T.);
#8638=EDGE_CURVE('',#7191,#7191,#6166,.T.);
#8639=EDGE_CURVE('',#7191,#7189,#4775,.T.);
#8640=EDGE_CURVE('',#7190,#7192,#4776,.T.);
#8641=EDGE_CURVE('',#7192,#7192,#6167,.T.);
#11402=ORIENTED_EDGE('',*,*,#8636,.F.);
#11403=ORIENTED_EDGE('',*,*,#8637,.T.);
#11404=ORIENTED_EDGE('',*,*,#8638,.F.);
#11405=ORIENTED_EDGE('',*,*,#8639,.T.);
#11406=ORIENTED_EDGE('',*,*,#8636,.T.);
#11407=ORIENTED_EDGE('',*,*,#8639,.F.);
#11408=ORIENTED_EDGE('',*,*,#8638,.T.);
#11409=ORIENTED_EDGE('',*,*,#8637,.F.);
#11410=ORIENTED_EDGE('',*,*,#8640,.T.);
#11411=ORIENTED_EDGE('',*,*,#8641,.T.);
#11412=ORIENTED_EDGE('',*,*,#8640,.F.);
#11413=ORIENTED_EDGE('',*,*,#8641,.F.);
#12343=CYLINDRICAL_SURFACE('',#15936,0.350000000000001);
#12344=CYLINDRICAL_SURFACE('',#15939,0.199999999999999);
#13051=ADVANCED_FACE('',(#2684,#1569),#1980,.F.);
#13052=ADVANCED_FACE('',(#2685),#12343,.T.);
#13053=ADVANCED_FACE('',(#2686),#1981,.T.);
#13054=ADVANCED_FACE('',(#2687),#12344,.T.);
#13055=ADVANCED_FACE('',(#2688),#1982,.F.);
#13335=CLOSED_SHELL('',(#13051,#13052,#13053,#13054,#13055));
#15932=AXIS2_PLACEMENT_3D('',#23834,#19813,#19814);
#15933=AXIS2_PLACEMENT_3D('',#23835,#19815,#19816);
#15934=AXIS2_PLACEMENT_3D('',#23837,#19817,#19818);
#15935=AXIS2_PLACEMENT_3D('',#23839,#19819,#19820);
#15936=AXIS2_PLACEMENT_3D('',#23840,#19821,#19822);
#15937=AXIS2_PLACEMENT_3D('',#23842,#19823,#19824);
#15938=AXIS2_PLACEMENT_3D('',#23844,#19826,#19827);
#15939=AXIS2_PLACEMENT_3D('',#23845,#19828,#19829);
#15940=AXIS2_PLACEMENT_3D('',#23848,#19831,#19832);
#15941=AXIS2_PLACEMENT_3D('',#23849,#19833,#19834);
#19813=DIRECTION('axis',(0.,0.,1.));
#19814=DIRECTION('refdir',(1.,0.,0.));
#19815=DIRECTION('center_axis',(0.,1.,0.));
#19816=DIRECTION('ref_axis',(1.,0.,0.));
#19817=DIRECTION('center_axis',(0.,1.,0.));
#19818=DIRECTION('ref_axis',(1.,0.,0.));
#19819=DIRECTION('center_axis',(0.,1.,0.));
#19820=DIRECTION('ref_axis',(1.,0.,0.));
#19821=DIRECTION('center_axis',(0.,1.,0.));
#19822=DIRECTION('ref_axis',(1.,0.,0.));
#19823=DIRECTION('center_axis',(0.,1.,0.));
#19824=DIRECTION('ref_axis',(1.,0.,0.));
#19825=DIRECTION('',(0.,-1.,0.));
#19826=DIRECTION('center_axis',(0.,1.,0.));
#19827=DIRECTION('ref_axis',(1.,0.,0.));
#19828=DIRECTION('center_axis',(0.,1.,0.));
#19829=DIRECTION('ref_axis',(1.,0.,0.));
#19830=DIRECTION('',(0.,-1.,0.));
#19831=DIRECTION('center_axis',(0.,1.,0.));
#19832=DIRECTION('ref_axis',(1.,0.,0.));
#19833=DIRECTION('center_axis',(0.,1.,0.));
#19834=DIRECTION('ref_axis',(1.,0.,0.));
#23834=CARTESIAN_POINT('',(0.,0.,0.));
#23835=CARTESIAN_POINT('Origin',(18.056769185842,-4.2,6.69185245480489));
#23836=CARTESIAN_POINT('',(17.706769185842,-4.2,6.69185245480489));
#23837=CARTESIAN_POINT('Origin',(18.056769185842,-4.2,6.69185245480489));
#23838=CARTESIAN_POINT('',(17.856769185842,-4.2,6.69185245480489));
#23839=CARTESIAN_POINT('Origin',(18.056769185842,-4.2,6.69185245480489));
#23840=CARTESIAN_POINT('Origin',(18.056769185842,-4.2,6.69185245480489));
#23841=CARTESIAN_POINT('',(17.706769185842,-4.1,6.69185245480489));
#23842=CARTESIAN_POINT('Origin',(18.056769185842,-4.1,6.69185245480489));
#23843=CARTESIAN_POINT('',(17.706769185842,-4.2,6.69185245480489));
#23844=CARTESIAN_POINT('Origin',(18.056769185842,-4.1,6.69185245480489));
#23845=CARTESIAN_POINT('Origin',(18.056769185842,-4.9,6.69185245480489));
#23846=CARTESIAN_POINT('',(17.856769185842,-4.9,6.69185245480489));
#23847=CARTESIAN_POINT('',(17.856769185842,-4.9,6.69185245480489));
#23848=CARTESIAN_POINT('Origin',(18.056769185842,-4.9,6.69185245480489));
#23849=CARTESIAN_POINT('Origin',(18.056769185842,-4.9,6.69185245480489));
#24951=UNCERTAINTY_MEASURE_WITH_UNIT(LENGTH_MEASURE(0.001),#25101,
'DISTANCE_ACCURACY_VALUE',
'Maximum model space distance between geometric entities at asserted c
onnectivities');
#24979=UNCERTAINTY_MEASURE_WITH_UNIT(LENGTH_MEASURE(0.001),#25101,
'DISTANCE_ACCURACY_VALUE',
'Maximum model space distance between geometric entities at asserted c
onnectivities');
#25072=(
GEOMETRIC_REPRESENTATION_CONTEXT(3)
GLOBAL_UNCERTAINTY_ASSIGNED_CONTEXT((#24951))
GLOBAL_UNIT_ASSIGNED_CONTEXT((#25101,#25103,#25104))
REPRESENTATION_CONTEXT('','3D')
);
#25100=(
GEOMETRIC_REPRESENTATION_CONTEXT(3)
GLOBAL_UNCERTAINTY_ASSIGNED_CONTEXT((#24979))
GLOBAL_UNIT_ASSIGNED_CONTEXT((#25101,#25103,#25104))
REPRESENTATION_CONTEXT('','3D')
);
#25101=(
LENGTH_UNIT()
NAMED_UNIT(*)
SI_UNIT(.CENTI.,.METRE.)
);
#25103=(
NAMED_UNIT(*)
PLANE_ANGLE_UNIT()
SI_UNIT($,.RADIAN.)
);
#25104=(
NAMED_UNIT(*)
SI_UNIT($,.STERADIAN.)
SOLID_ANGLE_UNIT()
);
#25197=SHAPE_DEFINITION_REPRESENTATION(#25391,#25602);
#25391=PRODUCT_DEFINITION_SHAPE('',$,#25723);
#25602=SHAPE_REPRESENTATION('',(#15932),#25072);
#25630=PRODUCT_DEFINITION_CONTEXT('part definition',#25992,'design');
#25723=PRODUCT_DEFINITION('M4 low-profile retaining screw (6)',
'M4 low-profile retaining screw (6)',#25843,#25630);
#25843=PRODUCT_DEFINITION_FORMATION('',$,#26086);
#25992=APPLICATION_CONTEXT(
'Core Data for Automotive Mechanical Design Process');
#25993=PRODUCT_CONTEXT('part definition',#25992,'mechanical');
#26086=PRODUCT('M4 low-profile retaining screw (6)',
'M4 low-profile retaining screw (6)','M4 low-profile retaining screw (6)',(#25993));
#26192=COLOUR_RGB('Black',0.12,0.14,0.17);
#26193=FILL_AREA_STYLE_COLOUR('',#26192);
#26194=FILL_AREA_STYLE('',(#26193));
#26195=SURFACE_STYLE_FILL_AREA(#26194);
#26196=SURFACE_SIDE_STYLE('',(#26195));
#26197=SURFACE_STYLE_USAGE(.BOTH.,#26196);
#26198=PRESENTATION_STYLE_ASSIGNMENT((#26197));
ENDSEC;
END-ISO-10303-21;
